ISO-10303-21;
HEADER;
/* Generated by software containing ST-Developer
 * from STEP Tools, Inc. (www.steptools.com) 
 */

FILE_DESCRIPTION(
/* description */ ('STEP AP214'),
/* implementation_level */ '2;1');

FILE_NAME(
/* name */ 'Lock Screw.step',
/* time_stamp */ '2026-11-14T06:58:01-08:00',
/* author */ (''),
/* organization */ (''),
/* preprocessor_version */ 'ST-DEVELOPER v20.2',
/* originating_system */ 'Autodesk Translation Framework v15.17.0.0',
/* authorisation */ '');

FILE_SCHEMA (('AUTOMOTIVE_DESIGN { 1 0 10303 214 3 1 1 }'));
ENDSEC;

DATA;
#10=MECHANICAL_DESIGN_GEOMETRIC_PRESENTATION_REPRESENTATION('',(#1157),#38635);
#154=TOROIDAL_SURFACE('',#18219,10.5,2.);
#881=FACE_BOUND('',#2914,.T.);
#882=FACE_BOUND('',#2916,.T.);
#1033=CONICAL_SURFACE('',#18224,4.25,0.643501108793284);
#1034=CONICAL_SURFACE('',#18230,5.,0.927295218001612);
#1123=SHAPE_REPRESENTATION_RELATIONSHIP('SRR','None',#38696,#1137);
#1137=ADVANCED_BREP_SHAPE_REPRESENTATION('',(#1183),#38632);
#1157=STYLED_ITEM('',(#38769),#1183);
#1183=MANIFOLD_SOLID_BREP('Body1',#17623);
#1271=PLANE('',#18240);
#1272=PLANE('',#18241);
#1273=PLANE('',#18242);
#1274=PLANE('',#18243);
#1880=FACE_OUTER_BOUND('',#2905,.T.);
#1881=FACE_OUTER_BOUND('',#2906,.T.);
#1882=FACE_OUTER_BOUND('',#2907,.T.);
#1883=FACE_OUTER_BOUND('',#2908,.T.);
#1884=FACE_OUTER_BOUND('',#2909,.T.);
#1885=FACE_OUTER_BOUND('',#2910,.T.);
#1886=FACE_OUTER_BOUND('',#2911,.T.);
#1887=FACE_OUTER_BOUND('',#2912,.T.);
#1888=FACE_OUTER_BOUND('',#2913,.T.);
#1889=FACE_OUTER_BOUND('',#2915,.T.);
#1890=FACE_OUTER_BOUND('',#2917,.T.);
#2905=EDGE_LOOP('',(#12029,#12030,#12031,#12032,#12033));
#2906=EDGE_LOOP('',(#12034,#12035,#12036,#12037));
#2907=EDGE_LOOP('',(#12038,#12039,#12040,#12041,#12042));
#2908=EDGE_LOOP('',(#12043,#12044,#12045,#12046,#12047,#12048));
#2909=EDGE_LOOP('',(#12049,#12050,#12051,#12052,#12053));
#2910=EDGE_LOOP('',(#12054,#12055,#12056,#12057));
#2911=EDGE_LOOP('',(#12058,#12059,#12060,#12061,#12062));
#2912=EDGE_LOOP('',(#12063));
#2913=EDGE_LOOP('',(#12064));
#2914=EDGE_LOOP('',(#12065));
#2915=EDGE_LOOP('',(#12066));
#2916=EDGE_LOOP('',(#12067));
#2917=EDGE_LOOP('',(#12068));
#3912=LINE('',#33022,#4856);
#3913=LINE('',#33029,#4857);
#3914=LINE('',#33032,#4858);
#3915=LINE('',#33039,#4859);
#3916=LINE('',#33044,#4860);
#3917=LINE('',#33048,#4861);
#4856=VECTOR('',#20835,4.25);
#4857=VECTOR('',#20844,5.);
#4858=VECTOR('',#20847,5.);
#4859=VECTOR('',#20856,4.25);
#4860=VECTOR('',#20861,6.);
#4861=VECTOR('',#20866,12.5);
#5781=CIRCLE('',#18220,12.5);
#5782=CIRCLE('',#18221,12.5);
#5783=CIRCLE('',#18222,2.);
#5784=CIRCLE('',#18223,10.5);
#5785=CIRCLE('',#18225,5.);
#5786=CIRCLE('',#18226,4.25);
#5787=CIRCLE('',#18228,5.);
#5788=CIRCLE('',#18229,5.);
#5789=CIRCLE('',#18231,4.25);
#5790=CIRCLE('',#18232,4.25);
#5791=CIRCLE('',#18234,4.25);
#5792=CIRCLE('',#18236,6.);
#5793=CIRCLE('',#18237,6.);
#5794=CIRCLE('',#18239,12.5);
#6872=VERTEX_POINT('',#33011);
#6873=VERTEX_POINT('',#33012);
#6874=VERTEX_POINT('',#33015);
#6875=VERTEX_POINT('',#33019);
#6876=VERTEX_POINT('',#33021);
#6877=VERTEX_POINT('',#33025);
#6878=VERTEX_POINT('',#33026);
#6879=VERTEX_POINT('',#33031);
#6880=VERTEX_POINT('',#33033);
#6881=VERTEX_POINT('',#33037);
#6882=VERTEX_POINT('',#33041);
#6883=VERTEX_POINT('',#33043);
#6884=VERTEX_POINT('',#33047);
#8801=EDGE_CURVE('',#6872,#6873,#5781,.T.);
#8802=EDGE_CURVE('',#6873,#6872,#5782,.T.);
#8803=EDGE_CURVE('',#6873,#6874,#5783,.T.);
#8804=EDGE_CURVE('',#6874,#6874,#5784,.T.);
#8805=EDGE_CURVE('',#6875,#6875,#5785,.T.);
#8806=EDGE_CURVE('',#6875,#6876,#3912,.T.);
#8807=EDGE_CURVE('',#6876,#6876,#5786,.T.);
#8808=EDGE_CURVE('',#6877,#6878,#5787,.T.);
#8809=EDGE_CURVE('',#6878,#6877,#5788,.T.);
#8810=EDGE_CURVE('',#6878,#6875,#3913,.T.);
#8811=EDGE_CURVE('',#6877,#6879,#3914,.T.);
#8812=EDGE_CURVE('',#6880,#6879,#5789,.T.);
#8813=EDGE_CURVE('',#6879,#6880,#5790,.T.);
#8814=EDGE_CURVE('',#6881,#6881,#5791,.T.);
#8815=EDGE_CURVE('',#6881,#6880,#3915,.T.);
#8816=EDGE_CURVE('',#6882,#6882,#5792,.T.);
#8817=EDGE_CURVE('',#6882,#6883,#3916,.T.);
#8818=EDGE_CURVE('',#6883,#6883,#5793,.T.);
#8819=EDGE_CURVE('',#6872,#6884,#3917,.T.);
#8820=EDGE_CURVE('',#6884,#6884,#5794,.T.);
#12029=ORIENTED_EDGE('',*,*,#8801,.F.);
#12030=ORIENTED_EDGE('',*,*,#8802,.F.);
#12031=ORIENTED_EDGE('',*,*,#8803,.T.);
#12032=ORIENTED_EDGE('',*,*,#8804,.F.);
#12033=ORIENTED_EDGE('',*,*,#8803,.F.);
#12034=ORIENTED_EDGE('',*,*,#8805,.F.);
#12035=ORIENTED_EDGE('',*,*,#8806,.T.);
#12036=ORIENTED_EDGE('',*,*,#8807,.T.);
#12037=ORIENTED_EDGE('',*,*,#8806,.F.);
#12038=ORIENTED_EDGE('',*,*,#8808,.F.);
#12039=ORIENTED_EDGE('',*,*,#8809,.F.);
#12040=ORIENTED_EDGE('',*,*,#8810,.T.);
#12041=ORIENTED_EDGE('',*,*,#8805,.T.);
#12042=ORIENTED_EDGE('',*,*,#8810,.F.);
#12043=ORIENTED_EDGE('',*,*,#8808,.T.);
#12044=ORIENTED_EDGE('',*,*,#8809,.T.);
#12045=ORIENTED_EDGE('',*,*,#8811,.T.);
#12046=ORIENTED_EDGE('',*,*,#8812,.F.);
#12047=ORIENTED_EDGE('',*,*,#8813,.F.);
#12048=ORIENTED_EDGE('',*,*,#8811,.F.);
#12049=ORIENTED_EDGE('',*,*,#8814,.F.);
#12050=ORIENTED_EDGE('',*,*,#8815,.T.);
#12051=ORIENTED_EDGE('',*,*,#8812,.T.);
#12052=ORIENTED_EDGE('',*,*,#8813,.T.);
#12053=ORIENTED_EDGE('',*,*,#8815,.F.);
#12054=ORIENTED_EDGE('',*,*,#8816,.F.);
#12055=ORIENTED_EDGE('',*,*,#8817,.T.);
#12056=ORIENTED_EDGE('',*,*,#8818,.T.);
#12057=ORIENTED_EDGE('',*,*,#8817,.F.);
#12058=ORIENTED_EDGE('',*,*,#8801,.T.);
#12059=ORIENTED_EDGE('',*,*,#8802,.T.);
#12060=ORIENTED_EDGE('',*,*,#8819,.T.);
#12061=ORIENTED_EDGE('',*,*,#8820,.T.);
#12062=ORIENTED_EDGE('',*,*,#8819,.F.);
#12063=ORIENTED_EDGE('',*,*,#8804,.T.);
#12064=ORIENTED_EDGE('',*,*,#8820,.F.);
#12065=ORIENTED_EDGE('',*,*,#8816,.T.);
#12066=ORIENTED_EDGE('',*,*,#8818,.F.);
#12067=ORIENTED_EDGE('',*,*,#8814,.T.);
#12068=ORIENTED_EDGE('',*,*,#8807,.F.);
#16345=CYLINDRICAL_SURFACE('',#18227,5.);
#16346=CYLINDRICAL_SURFACE('',#18233,4.25);
#16347=CYLINDRICAL_SURFACE('',#18235,6.);
#16348=CYLINDRICAL_SURFACE('',#18238,12.5);
#16839=ADVANCED_FACE('',(#1880),#154,.T.);
#16840=ADVANCED_FACE('',(#1881),#1033,.T.);
#16841=ADVANCED_FACE('',(#1882),#16345,.T.);
#16842=ADVANCED_FACE('',(#1883),#1034,.T.);
#16843=ADVANCED_FACE('',(#1884),#16346,.T.);
#16844=ADVANCED_FACE('',(#1885),#16347,.T.);
#16845=ADVANCED_FACE('',(#1886),#16348,.T.);
#16846=ADVANCED_FACE('',(#1887),#1271,.F.);
#16847=ADVANCED_FACE('',(#1888,#881),#1272,.F.);
#16848=ADVANCED_FACE('',(#1889,#882),#1273,.F.);
#16849=ADVANCED_FACE('',(#1890),#1274,.F.);
#17623=CLOSED_SHELL('',(#16839,#16840,#16841,#16842,#16843,#16844,#16845,
#16846,#16847,#16848,#16849));
#18218=AXIS2_PLACEMENT_3D('',#33009,#20819,#20820);
#18219=AXIS2_PLACEMENT_3D('',#33010,#20821,#20822);
#18220=AXIS2_PLACEMENT_3D('',#33013,#20823,#20824);
#18221=AXIS2_PLACEMENT_3D('',#33014,#20825,#20826);
#18222=AXIS2_PLACEMENT_3D('',#33016,#20827,#20828);
#18223=AXIS2_PLACEMENT_3D('',#33017,#20829,#20830);
#18224=AXIS2_PLACEMENT_3D('',#33018,#20831,#20832);
#18225=AXIS2_PLACEMENT_3D('',#33020,#20833,#20834);
#18226=AXIS2_PLACEMENT_3D('',#33023,#20836,#20837);
#18227=AXIS2_PLACEMENT_3D('',#33024,#20838,#20839);
#18228=AXIS2_PLACEMENT_3D('',#33027,#20840,#20841);
#18229=AXIS2_PLACEMENT_3D('',#33028,#20842,#20843);
#18230=AXIS2_PLACEMENT_3D('',#33030,#20845,#20846);
#18231=AXIS2_PLACEMENT_3D('',#33034,#20848,#20849);
#18232=AXIS2_PLACEMENT_3D('',#33035,#20850,#20851);
#18233=AXIS2_PLACEMENT_3D('',#33036,#20852,#20853);
#18234=AXIS2_PLACEMENT_3D('',#33038,#20854,#20855);
#18235=AXIS2_PLACEMENT_3D('',#33040,#20857,#20858);
#18236=AXIS2_PLACEMENT_3D('',#33042,#20859,#20860);
#18237=AXIS2_PLACEMENT_3D('',#33045,#20862,#20863);
#18238=AXIS2_PLACEMENT_3D('',#33046,#20864,#20865);
#18239=AXIS2_PLACEMENT_3D('',#33049,#20867,#20868);
#18240=AXIS2_PLACEMENT_3D('',#33050,#20869,#20870);
#18241=AXIS2_PLACEMENT_3D('',#33051,#20871,#20872);
#18242=AXIS2_PLACEMENT_3D('',#33052,#20873,#20874);
#18243=AXIS2_PLACEMENT_3D('',#33053,#20875,#20876);
#20819=DIRECTION('axis',(0.,0.,1.));
#20820=DIRECTION('refdir',(1.,0.,0.));
#20821=DIRECTION('center_axis',(1.,0.,0.));
#20822=DIRECTION('ref_axis',(0.,0.,-1.));
#20823=DIRECTION('center_axis',(1.,0.,0.));
#20824=DIRECTION('ref_axis',(0.,0.,-1.));
#20825=DIRECTION('center_axis',(1.,0.,0.));
#20826=DIRECTION('ref_axis',(0.,0.,-1.));
#20827=DIRECTION('center_axis',(0.,-1.,-1.22464679914735E-16));
#20828=DIRECTION('ref_axis',(0.,-1.22464679914735E-16,1.));
#20829=DIRECTION('center_axis',(-1.,0.,0.));
#20830=DIRECTION('ref_axis',(0.,0.,-1.));
#20831=DIRECTION('center_axis',(-1.,0.,0.));
#20832=DIRECTION('ref_axis',(0.,0.,1.));
#20833=DIRECTION('center_axis',(-1.,0.,0.));
#20834=DIRECTION('ref_axis',(0.,0.,1.));
#20835=DIRECTION('',(0.8,7.34788079488411E-17,0.6));
#20836=DIRECTION('center_axis',(-1.,0.,0.));
#20837=DIRECTION('ref_axis',(0.,0.,1.));
#20838=DIRECTION('center_axis',(-1.,0.,0.));
#20839=DIRECTION('ref_axis',(0.,0.,1.));
#20840=DIRECTION('center_axis',(-1.,0.,0.));
#20841=DIRECTION('ref_axis',(0.,0.,1.));
#20842=DIRECTION('center_axis',(-1.,0.,0.));
#20843=DIRECTION('ref_axis',(0.,0.,1.));
#20844=DIRECTION('',(1.,0.,0.));
#20845=DIRECTION('center_axis',(1.,0.,0.));
#20846=DIRECTION('ref_axis',(0.,0.,-1.));
#20847=DIRECTION('',(-0.600000000000001,9.79717439317882E-17,-0.8));
#20848=DIRECTION('center_axis',(-1.,0.,0.));
#20849=DIRECTION('ref_axis',(0.,0.,1.));
#20850=DIRECTION('center_axis',(-1.,0.,0.));
#20851=DIRECTION('ref_axis',(0.,0.,1.));
#20852=DIRECTION('center_axis',(-1.,0.,0.));
#20853=DIRECTION('ref_axis',(0.,0.,1.));
#20854=DIRECTION('center_axis',(-1.,0.,0.));
#20855=DIRECTION('ref_axis',(0.,0.,1.));
#20856=DIRECTION('',(1.,0.,0.));
#20857=DIRECTION('center_axis',(-1.,0.,0.));
#20858=DIRECTION('ref_axis',(0.,0.,1.));
#20859=DIRECTION('center_axis',(-1.,0.,0.));
#20860=DIRECTION('ref_axis',(0.,0.,1.));
#20861=DIRECTION('',(1.,0.,0.));
#20862=DIRECTION('center_axis',(-1.,0.,0.));
#20863=DIRECTION('ref_axis',(0.,0.,1.));
#20864=DIRECTION('center_axis',(-1.,0.,0.));
#20865=DIRECTION('ref_axis',(0.,0.,1.));
#20866=DIRECTION('',(1.,0.,0.));
#20867=DIRECTION('center_axis',(-1.,0.,0.));
#20868=DIRECTION('ref_axis',(0.,0.,1.));
#20869=DIRECTION('center_axis',(1.,0.,0.));
#20870=DIRECTION('ref_axis',(0.,0.,-1.));
#20871=DIRECTION('center_axis',(-1.,0.,0.));
#20872=DIRECTION('ref_axis',(0.,0.,1.));
#20873=DIRECTION('center_axis',(-1.,0.,0.));
#20874=DIRECTION('ref_axis',(0.,0.,1.));
#20875=DIRECTION('center_axis',(-1.,0.,0.));
#20876=DIRECTION('ref_axis',(0.,0.,1.));
#33009=CARTESIAN_POINT('',(0.,0.,0.));
#33010=CARTESIAN_POINT('Origin',(2.,0.,0.));
#33011=CARTESIAN_POINT('',(2.,1.53080849893419E-15,-12.5));
#33012=CARTESIAN_POINT('',(2.,-1.53080849893419E-15,12.5));
#33013=CARTESIAN_POINT('Origin',(2.,0.,0.));
#33014=CARTESIAN_POINT('Origin',(2.,0.,0.));
#33015=CARTESIAN_POINT('',(0.,-1.28587913910472E-15,10.5));
#33016=CARTESIAN_POINT('Origin',(2.,-1.28587913910472E-15,10.5));
#33017=CARTESIAN_POINT('Origin',(0.,0.,0.));
#33018=CARTESIAN_POINT('Origin',(60.,0.,0.));
#33019=CARTESIAN_POINT('',(59.,-6.12323399573676E-16,-5.));
#33020=CARTESIAN_POINT('Origin',(59.,0.,0.));
#33021=CARTESIAN_POINT('',(60.,-5.20474889637625E-16,-4.25));
#33022=CARTESIAN_POINT('',(60.,-5.20474889637625E-16,-4.25));
#33023=CARTESIAN_POINT('Origin',(60.,0.,0.));
#33024=CARTESIAN_POINT('Origin',(0.,0.,0.));
#33025=CARTESIAN_POINT('',(50.0625,6.12323399573677E-16,5.));
#33026=CARTESIAN_POINT('',(50.0625,-6.12323399573677E-16,-5.));
#33027=CARTESIAN_POINT('Origin',(50.0625,0.,0.));
#33028=CARTESIAN_POINT('Origin',(50.0625,0.,0.));
#33029=CARTESIAN_POINT('',(0.,-6.12323399573677E-16,-5.));
#33030=CARTESIAN_POINT('Origin',(50.0625,0.,0.));
#33031=CARTESIAN_POINT('',(49.5,-5.20474889637625E-16,4.25));
#33032=CARTESIAN_POINT('',(50.0625,-6.12323399573677E-16,5.));
#33033=CARTESIAN_POINT('',(49.5,5.20474889637625E-16,-4.25));
#33034=CARTESIAN_POINT('Origin',(49.5,0.,0.));
#33035=CARTESIAN_POINT('Origin',(49.5,0.,0.));
#33036=CARTESIAN_POINT('Origin',(0.,0.,0.));
#33037=CARTESIAN_POINT('',(46.5,-5.20474889637625E-16,-4.25));
#33038=CARTESIAN_POINT('Origin',(46.5,0.,0.));
#33039=CARTESIAN_POINT('',(0.,-5.20474889637625E-16,-4.25));
#33040=CARTESIAN_POINT('Origin',(0.,0.,0.));
#33041=CARTESIAN_POINT('',(8.,-7.34788079488412E-16,-6.));
#33042=CARTESIAN_POINT('Origin',(8.,0.,0.));
#33043=CARTESIAN_POINT('',(46.5,-7.34788079488412E-16,-6.));
#33044=CARTESIAN_POINT('',(0.,-7.34788079488412E-16,-6.));
#33045=CARTESIAN_POINT('Origin',(46.5,0.,0.));
#33046=CARTESIAN_POINT('Origin',(0.,0.,0.));
#33047=CARTESIAN_POINT('',(8.,-1.53080849893419E-15,-12.5));
#33048=CARTESIAN_POINT('',(0.,-1.53080849893419E-15,-12.5));
#33049=CARTESIAN_POINT('Origin',(8.,0.,0.));
#33050=CARTESIAN_POINT('Origin',(0.,0.,0.));
#33051=CARTESIAN_POINT('Origin',(8.,12.5,0.));
#33052=CARTESIAN_POINT('Origin',(46.5,6.,0.));
#33053=CARTESIAN_POINT('Origin',(60.,4.25,0.));
#38616=UNCERTAINTY_MEASURE_WITH_UNIT(LENGTH_MEASURE(0.01),#38636,
'DISTANCE_ACCURACY_VALUE',
'Maximum model space distance between geometric entities at asserted c
onnectivities');
#38619=UNCERTAINTY_MEASURE_WITH_UNIT(LENGTH_MEASURE(0.01),#38636,
'DISTANCE_ACCURACY_VALUE',
'Maximum model space distance between geometric entities at asserted c
onnectivities');
#38632=(
GEOMETRIC_REPRESENTATION_CONTEXT(3)
GLOBAL_UNCERTAINTY_ASSIGNED_CONTEXT((#38616))
GLOBAL_UNIT_ASSIGNED_CONTEXT((#38636,#38638,#38639))
REPRESENTATION_CONTEXT('','3D')
);
#38635=(
GEOMETRIC_REPRESENTATION_CONTEXT(3)
GLOBAL_UNCERTAINTY_ASSIGNED_CONTEXT((#38619))
GLOBAL_UNIT_ASSIGNED_CONTEXT((#38636,#38638,#38639))
REPRESENTATION_CONTEXT('','3D')
);
#38636=(
LENGTH_UNIT()
NAMED_UNIT(*)
SI_UNIT(.MILLI.,.METRE.)
);
#38638=(
NAMED_UNIT(*)
PLANE_ANGLE_UNIT()
SI_UNIT($,.RADIAN.)
);
#38639=(
NAMED_UNIT(*)
SI_UNIT($,.STERADIAN.)
SOLID_ANGLE_UNIT()
);
#38652=SHAPE_DEFINITION_REPRESENTATION(#38667,#38696);
#38667=PRODUCT_DEFINITION_SHAPE('',$,#38712);
#38696=SHAPE_REPRESENTATION('',(#18218),#38632);
#38699=PRODUCT_DEFINITION_CONTEXT('part definition',#38746,'design');
#38712=PRODUCT_DEFINITION('Lock Screw','Lock Screw',#38727,#38699);
#38727=PRODUCT_DEFINITION_FORMATION('',$,#38760);
#38746=APPLICATION_CONTEXT(
'Core Data for Automotive Mechanical Design Process');
#38747=PRODUCT_CONTEXT('part definition',#38746,'mechanical');
#38760=PRODUCT('Lock Screw','Lock Screw',$,(#38747));
#38769=PRESENTATION_STYLE_ASSIGNMENT((#38776));
#38776=SURFACE_STYLE_USAGE(.BOTH.,#38783);
#38783=SURFACE_SIDE_STYLE('',(#38790));
#38790=SURFACE_STYLE_FILL_AREA(#38797);
#38797=FILL_AREA_STYLE('Opaque(31,36,43)',(#38804));
#38804=FILL_AREA_STYLE_COLOUR('Opaque(31,36,43)',#38811);
#38811=COLOUR_RGB('Opaque(31,36,43)',0.12156862745098,0.141176470588235,
0.168627450980392);
ENDSEC;
END-ISO-10303-21;
